ISO-10303-21;
HEADER;
FILE_DESCRIPTION (('STEP AP214'),
    '1' );
FILE_NAME ('plain washer hardened_iso_Washer ISO 7415 - 30.step',
    '2026-10-02T18:08:48',
    ( '' ),
    ( '' ),
    'SwSTEP 2.0',
    'SolidWorks 2026',
    '' );
FILE_SCHEMA (( 'AUTOMOTIVE_DESIGN' ));
ENDSEC;

DATA;
#336=PLANE ( 'NONE',  #21046 ) ;
#350=ORIENTED_EDGE ( 'NONE', *, *, #18271, .F. ) ;
#371=CARTESIAN_POINT ( 'NONE',  ( -4.000000000000003553, 0.000000000000000000, 16.50000000000002842 ) ) ;
#388=FACE_OUTER_BOUND ( 'NONE', #6392, .T. ) ;
#556=ORIENTED_EDGE ( 'NONE', *, *, #8453, .F. ) ;
#637=MECHANICAL_DESIGN_GEOMETRIC_PRESENTATION_REPRESENTATION('',(#24223),#24742);
#1150=( NAMED_UNIT ( * ) PLANE_ANGLE_UNIT ( ) SI_UNIT ( $, .RADIAN. ) );
#1376=AXIS2_PLACEMENT_3D ( 'NONE', #6186, #27460, #21818 ) ;
#1598=ORIENTED_EDGE ( 'NONE', *, *, #25617, .F. ) ;
#1661=( LENGTH_UNIT ( ) NAMED_UNIT ( * ) SI_UNIT ( .MILLI., .METRE. ) );
#1776=CYLINDRICAL_SURFACE ( 'NONE', #28573, 16.50000000000002842 ) ;
#1914=DIRECTION ( 'NONE',  ( 0.000000000000000000, 0.000000000000000000, 1.000000000000000000 ) ) ;
#1930=ORIENTED_EDGE ( 'NONE', *, *, #18271, .T. ) ;
#2104=DIRECTION ( 'NONE',  ( 0.000000000000000000, 0.000000000000000000, 1.000000000000000000 ) ) ;
#2287=PRODUCT_DEFINITION_CONTEXT ( 'detailed design', #5501, 'design' ) ;
#2342=ORIENTED_EDGE ( 'NONE', *, *, #24940, .F. ) ;
#2418=FACE_OUTER_BOUND ( 'NONE', #11699, .T. ) ;
#2498=PRODUCT_DEFINITION_SHAPE ( 'NONE', 'NONE',  #23384 ) ;
#2651=APPLICATION_CONTEXT ( 'automotive_design' ) ;
#3158=ORIENTED_EDGE ( 'NONE', *, *, #25617, .T. ) ;
#3172=CARTESIAN_POINT ( 'NONE',  ( -34.92499999999992610, 0.000000000000000000, 0.000000000000000000 ) ) ;
#3333=DIRECTION ( 'NONE',  ( 0.000000000000000000, 0.000000000000000000, 1.000000000000000000 ) ) ;
#3355=ORIENTED_EDGE ( 'NONE', *, *, #12398, .F. ) ;
#3579=FILL_AREA_STYLE_COLOUR ( '', #8470 ) ;
#3631=CARTESIAN_POINT ( 'NONE',  ( -4.000000000000003553, 2.020667218593133100E-15, -16.50000000000000000 ) ) ;
#3939=CARTESIAN_POINT ( 'NONE',  ( -34.92499999999992610, 0.000000000000000000, 0.000000000000000000 ) ) ;
#3984=EDGE_LOOP ( 'NONE', ( #2342, #1598 ) ) ;
#4018=CARTESIAN_POINT ( 'NONE',  ( -34.92499999999992610, 0.000000000000000000, 16.50000000000002842 ) ) ;
#4359=DIRECTION ( 'NONE',  ( -1.000000000000000000, 0.000000000000000000, 0.000000000000000000 ) ) ;
#4443=DIRECTION ( 'NONE',  ( 0.000000000000000000, 0.000000000000000000, 1.000000000000000000 ) ) ;
#4483=DIRECTION ( 'NONE',  ( -1.000000000000000000, 0.000000000000000000, 0.000000000000000000 ) ) ;
#4538=EDGE_LOOP ( 'NONE', ( #3355, #32044 ) ) ;
#4680=CARTESIAN_POINT ( 'NONE',  ( 0.000000000000000000, 0.000000000000000000, 0.000000000000000000 ) ) ;
#4908=EDGE_CURVE ( 'NONE', #22684, #15950, #23655, .T. ) ;
#5086=VERTEX_POINT ( 'NONE', #16273 ) ;
#5501=APPLICATION_CONTEXT ( 'automotive_design' ) ;
#5555=CIRCLE ( 'NONE', #8285, 16.50000000000002842 ) ;
#5611=CARTESIAN_POINT ( 'NONE',  ( -4.000000000000003553, 0.000000000000000000, 0.000000000000000000 ) ) ;
#5807=EDGE_CURVE ( 'NONE', #27368, #25816, #24780, .T. ) ;
#6107=AXIS2_PLACEMENT_3D ( 'NONE', #21939, #32227, #8716 ) ;
#6186=CARTESIAN_POINT ( 'NONE',  ( 0.000000000000000000, 0.000000000000000000, 0.000000000000000000 ) ) ;
#6392=EDGE_LOOP ( 'NONE', ( #9816, #1930, #20649, #13067 ) ) ;
#6552=DIRECTION ( 'NONE',  ( 0.000000000000000000, 0.000000000000000000, 1.000000000000000000 ) ) ;
#6599=CARTESIAN_POINT ( 'NONE',  ( -34.92499999999992610, 0.000000000000000000, 0.000000000000000000 ) ) ;
#6895=CARTESIAN_POINT ( 'NONE',  ( 0.000000000000000000, 0.000000000000000000, 30.00000000000004974 ) ) ;
#6936=DIRECTION ( 'NONE',  ( 0.000000000000000000, 0.000000000000000000, 1.000000000000000000 ) ) ;
#6974=ADVANCED_FACE ( 'NONE', ( #30176 ), #16656, .T. ) ;
#7278=ORIENTED_EDGE ( 'NONE', *, *, #27657, .T. ) ;
#7332=PRESENTATION_STYLE_ASSIGNMENT (( #22957 ) ) ;
#7366=EDGE_CURVE ( 'NONE', #31472, #15743, #30745, .T. ) ;
#7369=( GEOMETRIC_REPRESENTATION_CONTEXT ( 3 ) GLOBAL_UNCERTAINTY_ASSIGNED_CONTEXT ( ( #8571 ) ) GLOBAL_UNIT_ASSIGNED_CONTEXT ( ( #1661, #22785, #30662 ) ) REPRESENTATION_CONTEXT ( 'NONE', 'WORKASPACE' ) );
#7632=SURFACE_STYLE_USAGE ( .BOTH. , #25489 ) ;
#7717=PRODUCT_CONTEXT ( 'NONE', #2651, 'mechanical' ) ;
#7800=( LENGTH_UNIT ( ) NAMED_UNIT ( * ) SI_UNIT ( .MILLI., .METRE. ) );
#7902=DIRECTION ( 'NONE',  ( 1.000000000000000000, 0.000000000000000000, 0.000000000000000000 ) ) ;
#8035=ADVANCED_FACE ( 'NONE', ( #14330 ), #1776, .F. ) ;
#8285=AXIS2_PLACEMENT_3D ( 'NONE', #5611, #26716, #10930 ) ;
#8302=DIRECTION ( 'NONE',  ( -1.000000000000000000, 0.000000000000000000, 0.000000000000000000 ) ) ;
#8351=AXIS2_PLACEMENT_3D ( 'NONE', #25074, #4483, #6552 ) ;
#8424=CIRCLE ( 'NONE', #12821, 30.00000000000004974 ) ;
#8453=EDGE_CURVE ( 'NONE', #15743, #31472, #11048, .T. ) ;
#8470=COLOUR_RGB ( '', 0.09019608, 0.27058824, 0.51372549) ;
#8571=UNCERTAINTY_MEASURE_WITH_UNIT (LENGTH_MEASURE( 1.000000000000000082E-05 ), #1661, 'distance_accuracy_value', 'NONE');
#8640=FACE_OUTER_BOUND ( 'NONE', #33617, .T. ) ;
#8658=DIRECTION ( 'NONE',  ( -1.000000000000000000, 0.000000000000000000, 0.000000000000000000 ) ) ;
#8716=DIRECTION ( 'NONE',  ( 0.000000000000000000, 0.000000000000000000, 1.000000000000000000 ) ) ;
#8720=( NAMED_UNIT ( * ) SI_UNIT ( $, .STERADIAN. ) SOLID_ANGLE_UNIT ( ) );
#8822=FACE_BOUND ( 'NONE', #11917, .T. ) ;
#8954=CYLINDRICAL_SURFACE ( 'NONE', #8351, 30.00000000000004974 ) ;
#9047=LINE ( 'NONE', #11296, #17290 ) ;
#9431=MANIFOLD_SOLID_BREP ( 'Base-Revolve', #27066 ) ;
#9501=ORIENTED_EDGE ( 'NONE', *, *, #8453, .T. ) ;
#9566=SHAPE_DEFINITION_REPRESENTATION ( #2498, #10290 ) ;
#9816=ORIENTED_EDGE ( 'NONE', *, *, #24940, .T. ) ;
#9885=PRODUCT_DEFINITION_FORMATION_WITH_SPECIFIED_SOURCE ( 'ANY', '', #27642, .NOT_KNOWN. ) ;
#10290=SHAPE_REPRESENTATION ( 'plain washer hardened_iso_Washer ISO 7415 - 30', ( #1376 ), #23828 ) ;
#10543=ORIENTED_EDGE ( 'NONE', *, *, #5807, .F. ) ;
#10735=DIRECTION ( 'NONE',  ( 0.000000000000000000, 0.000000000000000000, 1.000000000000000000 ) ) ;
#10861=VECTOR ( 'NONE', #19014, 1000.000000000000000 ) ;
#10930=DIRECTION ( 'NONE',  ( 0.000000000000000000, 0.000000000000000000, 1.000000000000000000 ) ) ;
#11048=CIRCLE ( 'NONE', #6107, 30.00000000000004974 ) ;
#11134=DIRECTION ( 'NONE',  ( -1.000000000000000000, 0.000000000000000000, 0.000000000000000000 ) ) ;
#11222=MECHANICAL_DESIGN_GEOMETRIC_PRESENTATION_REPRESENTATION('',(#28197),#7369);
#11296=CARTESIAN_POINT ( 'NONE',  ( -34.92499999999992610, 0.000000000000000000, 30.00000000000004974 ) ) ;
#11403=CARTESIAN_POINT ( 'NONE',  ( 0.000000000000000000, 16.50000000000002842, 0.000000000000000000 ) ) ;
#11699=EDGE_LOOP ( 'NONE', ( #13830, #9501 ) ) ;
#11917=EDGE_LOOP ( 'NONE', ( #7278, #31584 ) ) ;
#12223=CARTESIAN_POINT ( 'NONE',  ( 0.000000000000000000, 2.020667218593133100E-15, -16.50000000000000000 ) ) ;
#12229=DIRECTION ( 'NONE',  ( -1.000000000000000000, 0.000000000000000000, 0.000000000000000000 ) ) ;
#12269=AXIS2_PLACEMENT_3D ( 'NONE', #21212, #18303, #10735 ) ;
#12373=CARTESIAN_POINT ( 'NONE',  ( -34.92499999999992610, 3.673940397442066278E-15, -30.00000000000004974 ) ) ;
#12398=EDGE_CURVE ( 'NONE', #25816, #15950, #32111, .T. ) ;
#12488=SURFACE_STYLE_FILL_AREA ( #14051 ) ;
#12547=LINE ( 'NONE', #12373, #33482 ) ;
#12725=EDGE_CURVE ( 'NONE', #22684, #27368, #29196, .T. ) ;
#12801=AXIS2_PLACEMENT_3D ( 'NONE', #11403, #8658, #21880 ) ;
#12821=AXIS2_PLACEMENT_3D ( 'NONE', #4680, #12229, #2104 ) ;
#13067=ORIENTED_EDGE ( 'NONE', *, *, #33259, .F. ) ;
#13089=DIRECTION ( 'NONE',  ( -1.000000000000000000, 0.000000000000000000, 0.000000000000000000 ) ) ;
#13718=( LENGTH_UNIT ( ) NAMED_UNIT ( * ) SI_UNIT ( .MILLI., .METRE. ) );
#13830=ORIENTED_EDGE ( 'NONE', *, *, #7366, .T. ) ;
#14051=FILL_AREA_STYLE ('',( #3579 ) ) ;
#14330=FACE_OUTER_BOUND ( 'NONE', #25984, .T. ) ;
#14414=DIRECTION ( 'NONE',  ( -1.000000000000000000, 0.000000000000000000, 0.000000000000000000 ) ) ;
#15265=DIRECTION ( 'NONE',  ( -1.000000000000000000, 0.000000000000000000, 0.000000000000000000 ) ) ;
#15343=UNCERTAINTY_MEASURE_WITH_UNIT (LENGTH_MEASURE( 1.000000000000000082E-05 ), #13718, 'distance_accuracy_value', 'NONE');
#15743=VERTEX_POINT ( 'NONE', #23084 ) ;
#15912=ORIENTED_EDGE ( 'NONE', *, *, #33259, .T. ) ;
#15950=VERTEX_POINT ( 'NONE', #3631 ) ;
#16273=CARTESIAN_POINT ( 'NONE',  ( 0.000000000000000000, 3.673940397442059967E-15, -30.00000000000000000 ) ) ;
#16284=ORIENTED_EDGE ( 'NONE', *, *, #4908, .F. ) ;
#16656=CYLINDRICAL_SURFACE ( 'NONE', #18486, 30.00000000000004974 ) ;
#16906=EDGE_LOOP ( 'NONE', ( #350, #3158, #15912, #556 ) ) ;
#17290=VECTOR ( 'NONE', #11134, 1000.000000000000000 ) ;
#18077=CARTESIAN_POINT ( 'NONE',  ( -4.000000000000003553, 0.000000000000000000, 0.000000000000000000 ) ) ;
#18129=ADVANCED_BREP_SHAPE_REPRESENTATION ( '', ( #9431, #1376 ), #23828 ) ;
#18271=EDGE_CURVE ( 'NONE', #5086, #15743, #12547, .T. ) ;
#18303=DIRECTION ( 'NONE',  ( -1.000000000000000000, 0.000000000000000000, 0.000000000000000000 ) ) ;
#18423=DIRECTION ( 'NONE',  ( 0.000000000000000000, 0.000000000000000000, 1.000000000000000000 ) ) ;
#18486=AXIS2_PLACEMENT_3D ( 'NONE', #3939, #14414, #22464 ) ;
#19014=DIRECTION ( 'NONE',  ( -1.000000000000000000, 0.000000000000000000, 0.000000000000000000 ) ) ;
#19053=CARTESIAN_POINT ( 'NONE',  ( 0.000000000000000000, 0.000000000000000000, 0.000000000000000000 ) ) ;
#19062=ORIENTED_EDGE ( 'NONE', *, *, #12725, .F. ) ;
#19495=FILL_AREA_STYLE_COLOUR ( '', #31872 ) ;
#19856=ADVANCED_FACE ( 'NONE', ( #388 ), #8954, .T. ) ;
#20045=SURFACE_SIDE_STYLE ('',( #12488 ) ) ;
#20248=CARTESIAN_POINT ( 'NONE',  ( -4.000000000000003553, 0.000000000000000000, 0.000000000000000000 ) ) ;
#20649=ORIENTED_EDGE ( 'NONE', *, *, #7366, .F. ) ;
#20794=FACE_BOUND ( 'NONE', #4538, .T. ) ;
#20860=SURFACE_STYLE_FILL_AREA ( #23081 ) ;
#21046=AXIS2_PLACEMENT_3D ( 'NONE', #33648, #7902, #31572 ) ;
#21212=CARTESIAN_POINT ( 'NONE',  ( 0.000000000000000000, 0.000000000000000000, 0.000000000000000000 ) ) ;
#21299=DIRECTION ( 'NONE',  ( -1.000000000000000000, 0.000000000000000000, 0.000000000000000000 ) ) ;
#21723=ORIENTED_EDGE ( 'NONE', *, *, #27657, .F. ) ;
#21818=DIRECTION ( 'NONE',  ( 1.000000000000000000, 0.000000000000000000, 0.000000000000000000 ) ) ;
#21880=DIRECTION ( 'NONE',  ( 0.000000000000000000, 0.000000000000000000, 1.000000000000000000 ) ) ;
#21939=CARTESIAN_POINT ( 'NONE',  ( -4.000000000000003553, 0.000000000000000000, 0.000000000000000000 ) ) ;
#22250=EDGE_CURVE ( 'NONE', #15950, #25816, #5555, .T. ) ;
#22464=DIRECTION ( 'NONE',  ( 0.000000000000000000, 0.000000000000000000, 1.000000000000000000 ) ) ;
#22684=VERTEX_POINT ( 'NONE', #12223 ) ;
#22732=DIRECTION ( 'NONE',  ( -1.000000000000000000, 0.000000000000000000, 0.000000000000000000 ) ) ;
#22785=( NAMED_UNIT ( * ) PLANE_ANGLE_UNIT ( ) SI_UNIT ( $, .RADIAN. ) );
#22957=SURFACE_STYLE_USAGE ( .BOTH. , #20045 ) ;
#23081=FILL_AREA_STYLE ('',( #19495 ) ) ;
#23084=CARTESIAN_POINT ( 'NONE',  ( -4.000000000000003553, 3.673940397442059967E-15, -30.00000000000000000 ) ) ;
#23158=AXIS2_PLACEMENT_3D ( 'NONE', #27159, #24584, #1914 ) ;
#23259=( NAMED_UNIT ( * ) PLANE_ANGLE_UNIT ( ) SI_UNIT ( $, .RADIAN. ) );
#23384=PRODUCT_DEFINITION ( 'UNKNOWN', '', #9885, #2287 ) ;
#23655=LINE ( 'NONE', #26394, #10861 ) ;
#23828=( GEOMETRIC_REPRESENTATION_CONTEXT ( 3 ) GLOBAL_UNCERTAINTY_ASSIGNED_CONTEXT ( ( #15343 ) ) GLOBAL_UNIT_ASSIGNED_CONTEXT ( ( #13718, #1150, #8720 ) ) REPRESENTATION_CONTEXT ( 'NONE', 'WORKASPACE' ) );
#24223=STYLED_ITEM ( 'NONE', ( #33542 ), #9431 ) ;
#24584=DIRECTION ( 'NONE',  ( -1.000000000000000000, 0.000000000000000000, 0.000000000000000000 ) ) ;
#24742=( GEOMETRIC_REPRESENTATION_CONTEXT ( 3 ) GLOBAL_UNCERTAINTY_ASSIGNED_CONTEXT ( ( #32572 ) ) GLOBAL_UNIT_ASSIGNED_CONTEXT ( ( #7800, #23259, #30617 ) ) REPRESENTATION_CONTEXT ( 'NONE', 'WORKASPACE' ) );
#24780=LINE ( 'NONE', #4018, #33325 ) ;
#24940=EDGE_CURVE ( 'NONE', #27857, #5086, #25434, .T. ) ;
#25074=CARTESIAN_POINT ( 'NONE',  ( -34.92499999999992610, 0.000000000000000000, 0.000000000000000000 ) ) ;
#25357=CIRCLE ( 'NONE', #23158, 16.50000000000002842 ) ;
#25384=AXIS2_PLACEMENT_3D ( 'NONE', #3172, #8302, #3333 ) ;
#25434=CIRCLE ( 'NONE', #12269, 30.00000000000004974 ) ;
#25489=SURFACE_SIDE_STYLE ('',( #20860 ) ) ;
#25617=EDGE_CURVE ( 'NONE', #5086, #27857, #8424, .T. ) ;
#25674=CARTESIAN_POINT ( 'NONE',  ( -4.000000000000003553, 0.000000000000000000, 30.00000000000004974 ) ) ;
#25816=VERTEX_POINT ( 'NONE', #371 ) ;
#25984=EDGE_LOOP ( 'NONE', ( #19062, #27114, #31775, #10543 ) ) ;
#26394=CARTESIAN_POINT ( 'NONE',  ( -34.92499999999992610, 2.020667218593136255E-15, -16.50000000000002842 ) ) ;
#26716=DIRECTION ( 'NONE',  ( -1.000000000000000000, 0.000000000000000000, 0.000000000000000000 ) ) ;
#27066=CLOSED_SHELL ( 'NONE', ( #19856, #8035, #29083, #31783, #6974, #30118 ) ) ;
#27114=ORIENTED_EDGE ( 'NONE', *, *, #4908, .T. ) ;
#27159=CARTESIAN_POINT ( 'NONE',  ( 0.000000000000000000, 0.000000000000000000, 0.000000000000000000 ) ) ;
#27368=VERTEX_POINT ( 'NONE', #29058 ) ;
#27460=DIRECTION ( 'NONE',  ( 0.000000000000000000, 0.000000000000000000, 1.000000000000000000 ) ) ;
#27642=PRODUCT ( 'plain washer hardened_iso_Washer ISO 7415 - 30', 'plain washer hardened_iso_Washer ISO 7415 - 30', '', ( #7717 ) ) ;
#27657=EDGE_CURVE ( 'NONE', #27368, #22684, #25357, .T. ) ;
#27734=AXIS2_PLACEMENT_3D ( 'NONE', #18077, #13089, #18423 ) ;
#27857=VERTEX_POINT ( 'NONE', #6895 ) ;
#28095=AXIS2_PLACEMENT_3D ( 'NONE', #19053, #21299, #29492 ) ;
#28197=STYLED_ITEM ( 'NONE', ( #7332 ), #18129 ) ;
#28466=ORIENTED_EDGE ( 'NONE', *, *, #12398, .T. ) ;
#28573=AXIS2_PLACEMENT_3D ( 'NONE', #6599, #22732, #6936 ) ;
#29058=CARTESIAN_POINT ( 'NONE',  ( 0.000000000000000000, 0.000000000000000000, 16.50000000000002842 ) ) ;
#29083=ADVANCED_FACE ( 'NONE', ( #8640 ), #32311, .F. ) ;
#29093=ORIENTED_EDGE ( 'NONE', *, *, #5807, .T. ) ;
#29196=CIRCLE ( 'NONE', #28095, 16.50000000000002842 ) ;
#29492=DIRECTION ( 'NONE',  ( 0.000000000000000000, 0.000000000000000000, 1.000000000000000000 ) ) ;
#30118=ADVANCED_FACE ( 'NONE', ( #20794, #2418 ), #336, .F. ) ;
#30176=FACE_OUTER_BOUND ( 'NONE', #16906, .T. ) ;
#30617=( NAMED_UNIT ( * ) SI_UNIT ( $, .STERADIAN. ) SOLID_ANGLE_UNIT ( ) );
#30662=( NAMED_UNIT ( * ) SI_UNIT ( $, .STERADIAN. ) SOLID_ANGLE_UNIT ( ) );
#30745=CIRCLE ( 'NONE', #32408, 30.00000000000004974 ) ;
#31472=VERTEX_POINT ( 'NONE', #25674 ) ;
#31572=DIRECTION ( 'NONE',  ( -0.000000000000000000, 0.000000000000000000, -1.000000000000000000 ) ) ;
#31584=ORIENTED_EDGE ( 'NONE', *, *, #12725, .T. ) ;
#31775=ORIENTED_EDGE ( 'NONE', *, *, #22250, .T. ) ;
#31783=ADVANCED_FACE ( 'NONE', ( #32330, #8822 ), #32165, .F. ) ;
#31872=COLOUR_RGB ( '', 0.09019608, 0.27058824, 0.51372549) ;
#32044=ORIENTED_EDGE ( 'NONE', *, *, #22250, .F. ) ;
#32111=CIRCLE ( 'NONE', #27734, 16.50000000000002842 ) ;
#32165=PLANE ( 'NONE',  #12801 ) ;
#32227=DIRECTION ( 'NONE',  ( -1.000000000000000000, 0.000000000000000000, 0.000000000000000000 ) ) ;
#32311=CYLINDRICAL_SURFACE ( 'NONE', #25384, 16.50000000000002842 ) ;
#32330=FACE_OUTER_BOUND ( 'NONE', #3984, .T. ) ;
#32408=AXIS2_PLACEMENT_3D ( 'NONE', #20248, #15265, #4443 ) ;
#32572=UNCERTAINTY_MEASURE_WITH_UNIT (LENGTH_MEASURE( 1.000000000000000082E-05 ), #7800, 'distance_accuracy_value', 'NONE');
#33062=SHAPE_REPRESENTATION_RELATIONSHIP ( 'NONE' , 'NONE' ,  #10290, #18129 ) ;
#33259=EDGE_CURVE ( 'NONE', #27857, #31472, #9047, .T. ) ;
#33301=DIRECTION ( 'NONE',  ( -1.000000000000000000, 0.000000000000000000, 0.000000000000000000 ) ) ;
#33325=VECTOR ( 'NONE', #4359, 1000.000000000000000 ) ;
#33482=VECTOR ( 'NONE', #33301, 1000.000000000000000 ) ;
#33542=PRESENTATION_STYLE_ASSIGNMENT (( #7632 ) ) ;
#33617=EDGE_LOOP ( 'NONE', ( #16284, #21723, #29093, #28466 ) ) ;
#33648=CARTESIAN_POINT ( 'NONE',  ( -4.000000000000003553, 30.00000000000008171, -8.673617379884035472E-16 ) ) ;
ENDSEC;
END-ISO-10303-21;
